ISO-10303-21;
HEADER;
FILE_DESCRIPTION (('STEP AP214'),
    '1' );
FILE_NAME ('Part11^Assembly Idle gear.step',
    '2026-10-22T18:53:08',
    ( '' ),
    ( '' ),
    'SwSTEP 2.0',
    'SolidWorks 2025',
    '' );
FILE_SCHEMA (( 'AUTOMOTIVE_DESIGN' ));
ENDSEC;

DATA;
#299=EDGE_CURVE ( 'NONE', #3391, #4737, #19089, .T. ) ;
#344=LINE ( 'NONE', #20353, #1020 ) ;
#383=CONICAL_SURFACE ( 'NONE', #8934, 9.000000000000000000, 0.7853981633974473908 ) ;
#427=ADVANCED_FACE ( 'NONE', ( #9089 ), #383, .T. ) ;
#477=ORIENTED_EDGE ( 'NONE', *, *, #22323, .F. ) ;
#480=CYLINDRICAL_SURFACE ( 'NONE', #7582, 9.000000000000000000 ) ;
#711=DIRECTION ( 'NONE',  ( -0.000000000000000000, -0.000000000000000000, -1.000000000000000000 ) ) ;
#775=ORIENTED_EDGE ( 'NONE', *, *, #15208, .F. ) ;
#877=AXIS2_PLACEMENT_3D ( 'NONE', #20362, #14746, #3776 ) ;
#952=DIRECTION ( 'NONE',  ( 1.000000000000000000, 0.000000000000000000, 0.000000000000000000 ) ) ;
#1020=VECTOR ( 'NONE', #7871, 1000.000000000000000 ) ;
#1140=DIRECTION ( 'NONE',  ( 1.000000000000000000, 0.000000000000000000, -0.000000000000000000 ) ) ;
#1324=ORIENTED_EDGE ( 'NONE', *, *, #17103, .F. ) ;
#1459=LINE ( 'NONE', #5095, #23854 ) ;
#1627=DIRECTION ( 'NONE',  ( 1.000000000000000000, 0.000000000000000000, 0.000000000000000000 ) ) ;
#1651=ORIENTED_EDGE ( 'NONE', *, *, #19156, .T. ) ;
#1682=DIRECTION ( 'NONE',  ( 1.000000000000000000, 0.000000000000000000, 0.000000000000000000 ) ) ;
#1727=AXIS2_PLACEMENT_3D ( 'NONE', #14130, #21593, #12298 ) ;
#1783=PRODUCT_CONTEXT ( 'NONE', #18992, 'mechanical' ) ;
#1866=DIRECTION ( 'NONE',  ( 1.000000000000000000, 0.000000000000000000, -0.000000000000000000 ) ) ;
#1889=STYLED_ITEM('',(#24141),#2111);
#2068=EDGE_LOOP ( 'NONE', ( #7368, #2890, #16000, #16433 ) ) ;
#2111=MANIFOLD_SOLID_BREP ( 'Chamfer1', #11216 ) ;
#2185=PRODUCT_DEFINITION_FORMATION_WITH_SPECIFIED_SOURCE ( 'ANY', '', #4982, .NOT_KNOWN. ) ;
#2278=CARTESIAN_POINT ( 'NONE',  ( 0.000000000000000000, 0.000000000000000000, 51.99999999999998579 ) ) ;
#2352=EDGE_LOOP ( 'NONE', ( #7318, #18959, #10120, #775 ) ) ;
#2456=EDGE_CURVE ( 'NONE', #15497, #14826, #10290, .T. ) ;
#2575=( GEOMETRIC_REPRESENTATION_CONTEXT ( 3 ) GLOBAL_UNCERTAINTY_ASSIGNED_CONTEXT ( ( #3996 ) ) GLOBAL_UNIT_ASSIGNED_CONTEXT ( ( #19282, #6101, #10356 ) ) REPRESENTATION_CONTEXT ( 'NONE', 'WORKASPACE' ) );
#2617=PRODUCT_DEFINITION_CONTEXT ( 'detailed design', #3096, 'design' ) ;
#2665=EDGE_CURVE ( 'NONE', #23772, #21717, #18503, .T. ) ;
#2890=ORIENTED_EDGE ( 'NONE', *, *, #17103, .T. ) ;
#2979=DIRECTION ( 'NONE',  ( -0.000000000000000000, -0.000000000000000000, 1.000000000000000000 ) ) ;
#3096=APPLICATION_CONTEXT ( 'automotive_design' ) ;
#3253=DIRECTION ( 'NONE',  ( 1.000000000000000000, 0.000000000000000000, 0.000000000000000000 ) ) ;
#3391=VERTEX_POINT ( 'NONE', #18220 ) ;
#3451=( NAMED_UNIT ( * ) PLANE_ANGLE_UNIT ( ) SI_UNIT ( $, .RADIAN. ) );
#3467=CARTESIAN_POINT ( 'NONE',  ( 0.000000000000000000, 0.000000000000000000, 0.9999999999999940048 ) ) ;
#3554=( LENGTH_UNIT ( ) NAMED_UNIT ( * ) SI_UNIT ( .MILLI., .METRE. ) );
#3738=AXIS2_PLACEMENT_3D ( 'NONE', #10398, #12083, #1140 ) ;
#3776=DIRECTION ( 'NONE',  ( 1.000000000000000000, 0.000000000000000000, 0.000000000000000000 ) ) ;
#3985=AXIS2_PLACEMENT_3D ( 'NONE', #15340, #4522, #17171 ) ;
#3996=UNCERTAINTY_MEASURE_WITH_UNIT (LENGTH_MEASURE( 1.000000000000000082E-05 ), #19282, 'distance_accuracy_value', 'NONE');
#4063=ORIENTED_EDGE ( 'NONE', *, *, #15668, .T. ) ;
#4090=CIRCLE ( 'NONE', #9919, 9.000000000000000000 ) ;
#4291=AXIS2_PLACEMENT_3D ( 'NONE', #17648, #711, #952 ) ;
#4522=DIRECTION ( 'NONE',  ( -0.000000000000000000, -0.000000000000000000, -1.000000000000000000 ) ) ;
#4737=VERTEX_POINT ( 'NONE', #21627 ) ;
#4930=AXIS2_PLACEMENT_3D ( 'NONE', #19933, #18591, #1866 ) ;
#4982=PRODUCT ( 'Part11^Assembly Idle gear', 'Part11^Assembly Idle gear', '', ( #1783 ) ) ;
#5095=CARTESIAN_POINT ( 'NONE',  ( -9.000000000000000000, 1.102182119232617714E-15, 0.9999999999999940048 ) ) ;
#5156=PRODUCT_DEFINITION_SHAPE ( 'NONE', 'NONE',  #22438 ) ;
#5167=DIRECTION ( 'NONE',  ( -0.000000000000000000, -0.000000000000000000, -1.000000000000000000 ) ) ;
#5217=DIRECTION ( 'NONE',  ( -0.7071067811865469066, 8.659560562354926695E-17, 0.7071067811865482389 ) ) ;
#5295=CARTESIAN_POINT ( 'NONE',  ( 0.000000000000000000, 0.000000000000000000, 0.000000000000000000 ) ) ;
#5298=ORIENTED_EDGE ( 'NONE', *, *, #299, .T. ) ;
#5332=CARTESIAN_POINT ( 'NONE',  ( 0.000000000000000000, 0.000000000000000000, 0.9999999999999940048 ) ) ;
#5426=CARTESIAN_POINT ( 'NONE',  ( 7.999999999999986677, 9.797174393178809880E-16, 53.00000000000000000 ) ) ;
#5715=CARTESIAN_POINT ( 'NONE',  ( -7.999999999999986677, 0.000000000000000000, 53.00000000000000000 ) ) ;
#5798=SHAPE_DEFINITION_REPRESENTATION ( #5156, #23741 ) ;
#5976=CONICAL_SURFACE ( 'NONE', #6362, 9.000000000000000000, 0.7853981633974473908 ) ;
#5978=CARTESIAN_POINT ( 'NONE',  ( 0.000000000000000000, 0.000000000000000000, 0.000000000000000000 ) ) ;
#6006=CARTESIAN_POINT ( 'NONE',  ( 9.000000000000000000, 1.102182119232617714E-15, 0.9999999999999940048 ) ) ;
#6101=( NAMED_UNIT ( * ) PLANE_ANGLE_UNIT ( ) SI_UNIT ( $, .RADIAN. ) );
#6362=AXIS2_PLACEMENT_3D ( 'NONE', #3467, #10531, #14087 ) ;
#6497=ORIENTED_EDGE ( 'NONE', *, *, #2665, .F. ) ;
#6507=CIRCLE ( 'NONE', #16602, 7.999999999999986677 ) ;
#6540=DIRECTION ( 'NONE',  ( 0.000000000000000000, 0.000000000000000000, -1.000000000000000000 ) ) ;
#6673=ORIENTED_EDGE ( 'NONE', *, *, #22096, .F. ) ;
#6698=FACE_OUTER_BOUND ( 'NONE', #20074, .T. ) ;
#6977=CARTESIAN_POINT ( 'NONE',  ( -9.000000000000000000, 0.000000000000000000, 51.99999999999998579 ) ) ;
#7318=ORIENTED_EDGE ( 'NONE', *, *, #19156, .F. ) ;
#7342=PLANE ( 'NONE',  #4930 ) ;
#7352=LINE ( 'NONE', #12730, #11129 ) ;
#7368=ORIENTED_EDGE ( 'NONE', *, *, #15668, .F. ) ;
#7416=FACE_OUTER_BOUND ( 'NONE', #2068, .T. ) ;
#7513=ORIENTED_EDGE ( 'NONE', *, *, #18592, .T. ) ;
#7561=( NAMED_UNIT ( * ) SI_UNIT ( $, .STERADIAN. ) SOLID_ANGLE_UNIT ( ) );
#7582=AXIS2_PLACEMENT_3D ( 'NONE', #22680, #9484, #13040 ) ;
#7637=CONICAL_SURFACE ( 'NONE', #24016, 7.999999999999986677, 0.7853981633974473908 ) ;
#7644=UNCERTAINTY_MEASURE_WITH_UNIT (LENGTH_MEASURE( 1.000000000000000082E-05 ), #3554, 'distance_accuracy_value', 'NONE');
#7749=DIRECTION ( 'NONE',  ( 1.000000000000000000, 0.000000000000000000, 0.000000000000000000 ) ) ;
#7871=DIRECTION ( 'NONE',  ( -0.000000000000000000, -0.000000000000000000, -1.000000000000000000 ) ) ;
#7981=ORIENTED_EDGE ( 'NONE', *, *, #22449, .F. ) ;
#8005=AXIS2_PLACEMENT_3D ( 'NONE', #5978, #22344, #13412 ) ;
#8934=AXIS2_PLACEMENT_3D ( 'NONE', #12277, #23406, #19748 ) ;
#8977=DIRECTION ( 'NONE',  ( 0.000000000000000000, 0.000000000000000000, -1.000000000000000000 ) ) ;
#8998=ADVANCED_BREP_SHAPE_REPRESENTATION ( '', ( #2111, #8005 ), #2575 ) ;
#9028=ORIENTED_EDGE ( 'NONE', *, *, #9077, .F. ) ;
#9077=EDGE_CURVE ( 'NONE', #17802, #16134, #11741, .T. ) ;
#9089=FACE_OUTER_BOUND ( 'NONE', #2352, .T. ) ;
#9484=DIRECTION ( 'NONE',  ( -0.000000000000000000, -0.000000000000000000, -1.000000000000000000 ) ) ;
#9587=DIRECTION ( 'NONE',  ( -0.7071067811865469066, 0.000000000000000000, -0.7071067811865481278 ) ) ;
#9919=AXIS2_PLACEMENT_3D ( 'NONE', #2278, #16913, #7749 ) ;
#10043=FACE_OUTER_BOUND ( 'NONE', #13967, .T. ) ;
#10120=ORIENTED_EDGE ( 'NONE', *, *, #22449, .T. ) ;
#10290=CIRCLE ( 'NONE', #16525, 9.000000000000000000 ) ;
#10309=AXIS2_PLACEMENT_3D ( 'NONE', #12231, #2979, #16858 ) ;
#10335=ADVANCED_FACE ( 'NONE', ( #22811 ), #20862, .T. ) ;
#10356=( NAMED_UNIT ( * ) SI_UNIT ( $, .STERADIAN. ) SOLID_ANGLE_UNIT ( ) );
#10398=CARTESIAN_POINT ( 'NONE',  ( 0.000000000000000000, 0.000000000000000000, 0.000000000000000000 ) ) ;
#10531=DIRECTION ( 'NONE',  ( -0.000000000000000000, -0.000000000000000000, 1.000000000000000000 ) ) ;
#10553=CIRCLE ( 'NONE', #23823, 8.000000000000007105 ) ;
#10632=VECTOR ( 'NONE', #22949, 1000.000000000000000 ) ;
#10773=EDGE_LOOP ( 'NONE', ( #22967, #4063, #22385, #6673 ) ) ;
#10874=EDGE_LOOP ( 'NONE', ( #16673, #17245 ) ) ;
#11052=ORIENTED_EDGE ( 'NONE', *, *, #18592, .F. ) ;
#11129=VECTOR ( 'NONE', #22500, 999.9999999999998863 ) ;
#11216=CLOSED_SHELL ( 'NONE', ( #22202, #12056, #10335, #13178, #13615, #22822, #427, #20511 ) ) ;
#11741=CIRCLE ( 'NONE', #877, 7.999999999999986677 ) ;
#12056=ADVANCED_FACE ( 'NONE', ( #23267 ), #5976, .T. ) ;
#12083=DIRECTION ( 'NONE',  ( 0.000000000000000000, 0.000000000000000000, 1.000000000000000000 ) ) ;
#12110=DIRECTION ( 'NONE',  ( 0.000000000000000000, 0.000000000000000000, 1.000000000000000000 ) ) ;
#12231=CARTESIAN_POINT ( 'NONE',  ( 0.000000000000000000, 0.000000000000000000, 0.9999999999999940048 ) ) ;
#12277=CARTESIAN_POINT ( 'NONE',  ( 0.000000000000000000, 0.000000000000000000, 0.9999999999999940048 ) ) ;
#12298=DIRECTION ( 'NONE',  ( -1.000000000000000000, 0.000000000000000000, 0.000000000000000000 ) ) ;
#12730=CARTESIAN_POINT ( 'NONE',  ( 9.000000000000000000, 0.000000000000000000, 0.9999999999999940048 ) ) ;
#12846=DIRECTION ( 'NONE',  ( 0.7071067811865469066, 8.659560562354925463E-17, -0.7071067811865481278 ) ) ;
#13040=DIRECTION ( 'NONE',  ( -1.000000000000000000, 0.000000000000000000, 0.000000000000000000 ) ) ;
#13178=ADVANCED_FACE ( 'NONE', ( #7416 ), #480, .T. ) ;
#13398=CONICAL_SURFACE ( 'NONE', #1727, 7.999999999999986677, 0.7853981633974473908 ) ;
#13412=DIRECTION ( 'NONE',  ( 1.000000000000000000, 0.000000000000000000, 0.000000000000000000 ) ) ;
#13615=ADVANCED_FACE ( 'NONE', ( #24065 ), #7342, .T. ) ;
#13915=SHAPE_REPRESENTATION_RELATIONSHIP ( 'NONE' , 'NONE' ,  #23741, #8998 ) ;
#13921=CARTESIAN_POINT ( 'NONE',  ( 9.000000000000000000, 1.102182119232617714E-15, 53.00000000000000000 ) ) ;
#13967=EDGE_LOOP ( 'NONE', ( #9028, #23986, #21594, #16065 ) ) ;
#14014=EDGE_LOOP ( 'NONE', ( #5298, #7513 ) ) ;
#14087=DIRECTION ( 'NONE',  ( 1.000000000000000000, 0.000000000000000000, 0.000000000000000000 ) ) ;
#14130=CARTESIAN_POINT ( 'NONE',  ( 0.000000000000000000, 0.000000000000000000, 53.00000000000000000 ) ) ;
#14745=EDGE_CURVE ( 'NONE', #17802, #14826, #18242, .T. ) ;
#14746=DIRECTION ( 'NONE',  ( 0.000000000000000000, 0.000000000000000000, 1.000000000000000000 ) ) ;
#14826=VERTEX_POINT ( 'NONE', #16091 ) ;
#15112=MECHANICAL_DESIGN_GEOMETRIC_PRESENTATION_REPRESENTATION('',(#1889),#20600);
#15208=EDGE_CURVE ( 'NONE', #21717, #23772, #22805, .T. ) ;
#15340=CARTESIAN_POINT ( 'NONE',  ( 0.000000000000000000, 0.000000000000000000, 53.00000000000000000 ) ) ;
#15497=VERTEX_POINT ( 'NONE', #6977 ) ;
#15668=EDGE_CURVE ( 'NONE', #14826, #23772, #19048, .T. ) ;
#16000=ORIENTED_EDGE ( 'NONE', *, *, #22096, .T. ) ;
#16065=ORIENTED_EDGE ( 'NONE', *, *, #17053, .F. ) ;
#16091=CARTESIAN_POINT ( 'NONE',  ( 9.000000000000000000, 1.102182119232617714E-15, 51.99999999999998579 ) ) ;
#16129=PLANE ( 'NONE',  #3738 ) ;
#16134=VERTEX_POINT ( 'NONE', #21697 ) ;
#16271=CARTESIAN_POINT ( 'NONE',  ( 0.000000000000000000, 0.000000000000000000, 53.00000000000000000 ) ) ;
#16433=ORIENTED_EDGE ( 'NONE', *, *, #15208, .T. ) ;
#16525=AXIS2_PLACEMENT_3D ( 'NONE', #18388, #8977, #1682 ) ;
#16602=AXIS2_PLACEMENT_3D ( 'NONE', #16271, #12110, #23622 ) ;
#16663=DIRECTION ( 'NONE',  ( -0.000000000000000000, -0.000000000000000000, 1.000000000000000000 ) ) ;
#16673=ORIENTED_EDGE ( 'NONE', *, *, #22323, .T. ) ;
#16790=ORIENTED_EDGE ( 'NONE', *, *, #14745, .F. ) ;
#16858=DIRECTION ( 'NONE',  ( 1.000000000000000000, 0.000000000000000000, 0.000000000000000000 ) ) ;
#16913=DIRECTION ( 'NONE',  ( 0.000000000000000000, 0.000000000000000000, -1.000000000000000000 ) ) ;
#17053=EDGE_CURVE ( 'NONE', #16134, #15497, #22432, .T. ) ;
#17103=EDGE_CURVE ( 'NONE', #14826, #15497, #4090, .T. ) ;
#17171=DIRECTION ( 'NONE',  ( -1.000000000000000000, 0.000000000000000000, 0.000000000000000000 ) ) ;
#17245=ORIENTED_EDGE ( 'NONE', *, *, #9077, .T. ) ;
#17499=DIRECTION ( 'NONE',  ( -1.000000000000000000, 0.000000000000000000, 0.000000000000000000 ) ) ;
#17648=CARTESIAN_POINT ( 'NONE',  ( 0.000000000000000000, 0.000000000000000000, 0.000000000000000000 ) ) ;
#17802=VERTEX_POINT ( 'NONE', #18109 ) ;
#17852=FACE_OUTER_BOUND ( 'NONE', #14014, .T. ) ;
#18109=CARTESIAN_POINT ( 'NONE',  ( 7.999999999999986677, 1.040949779275249548E-15, 53.00000000000000000 ) ) ;
#18126=AXIS2_PLACEMENT_3D ( 'NONE', #5332, #16663, #3253 ) ;
#18220=CARTESIAN_POINT ( 'NONE',  ( 8.000000000000007105, 0.000000000000000000, 0.000000000000000000 ) ) ;
#18242=LINE ( 'NONE', #5426, #20886 ) ;
#18388=CARTESIAN_POINT ( 'NONE',  ( 0.000000000000000000, 0.000000000000000000, 51.99999999999998579 ) ) ;
#18503=CIRCLE ( 'NONE', #10309, 9.000000000000000000 ) ;
#18591=DIRECTION ( 'NONE',  ( 0.000000000000000000, 0.000000000000000000, 1.000000000000000000 ) ) ;
#18592=EDGE_CURVE ( 'NONE', #4737, #3391, #10553, .T. ) ;
#18891=VECTOR ( 'NONE', #9587, 1000.000000000000114 ) ;
#18959=ORIENTED_EDGE ( 'NONE', *, *, #299, .F. ) ;
#18992=APPLICATION_CONTEXT ( 'automotive_design' ) ;
#19048=LINE ( 'NONE', #13921, #10632 ) ;
#19089=CIRCLE ( 'NONE', #4291, 8.000000000000007105 ) ;
#19156=EDGE_CURVE ( 'NONE', #4737, #21717, #1459, .T. ) ;
#19282=( LENGTH_UNIT ( ) NAMED_UNIT ( * ) SI_UNIT ( .MILLI., .METRE. ) );
#19748=DIRECTION ( 'NONE',  ( 1.000000000000000000, 0.000000000000000000, 0.000000000000000000 ) ) ;
#19933=CARTESIAN_POINT ( 'NONE',  ( 0.000000000000000000, 0.000000000000000000, 53.00000000000000000 ) ) ;
#20040=EDGE_LOOP ( 'NONE', ( #11052, #1651, #6497, #7981 ) ) ;
#20074=EDGE_LOOP ( 'NONE', ( #16790, #477, #22530, #1324 ) ) ;
#20353=CARTESIAN_POINT ( 'NONE',  ( -9.000000000000000000, 0.000000000000000000, 53.00000000000000000 ) ) ;
#20362=CARTESIAN_POINT ( 'NONE',  ( 0.000000000000000000, 0.000000000000000000, 53.00000000000000000 ) ) ;
#20511=ADVANCED_FACE ( 'NONE', ( #6698 ), #13398, .T. ) ;
#20600=( GEOMETRIC_REPRESENTATION_CONTEXT ( 3 ) GLOBAL_UNCERTAINTY_ASSIGNED_CONTEXT ( ( #7644 ) ) GLOBAL_UNIT_ASSIGNED_CONTEXT ( ( #3554, #3451, #7561 ) ) REPRESENTATION_CONTEXT ( 'NONE', 'WORKASPACE' ) );
#20862=CYLINDRICAL_SURFACE ( 'NONE', #3985, 9.000000000000000000 ) ;
#20886=VECTOR ( 'NONE', #12846, 1000.000000000000114 ) ;
#21593=DIRECTION ( 'NONE',  ( 0.000000000000000000, 0.000000000000000000, -1.000000000000000000 ) ) ;
#21594=ORIENTED_EDGE ( 'NONE', *, *, #2456, .F. ) ;
#21627=CARTESIAN_POINT ( 'NONE',  ( -8.000000000000007105, 1.040949779275250534E-15, 0.000000000000000000 ) ) ;
#21697=CARTESIAN_POINT ( 'NONE',  ( -7.999999999999986677, 0.000000000000000000, 53.00000000000000000 ) ) ;
#21717=VERTEX_POINT ( 'NONE', #23434 ) ;
#22096=EDGE_CURVE ( 'NONE', #15497, #21717, #344, .T. ) ;
#22202=ADVANCED_FACE ( 'NONE', ( #10043 ), #7637, .T. ) ;
#22323=EDGE_CURVE ( 'NONE', #16134, #17802, #6507, .T. ) ;
#22344=DIRECTION ( 'NONE',  ( 0.000000000000000000, 0.000000000000000000, 1.000000000000000000 ) ) ;
#22385=ORIENTED_EDGE ( 'NONE', *, *, #2665, .T. ) ;
#22432=LINE ( 'NONE', #5715, #18891 ) ;
#22438=PRODUCT_DEFINITION ( 'UNKNOWN', '', #2185, #2617 ) ;
#22449=EDGE_CURVE ( 'NONE', #3391, #23772, #7352, .T. ) ;
#22500=DIRECTION ( 'NONE',  ( 0.7071067811865469066, 0.000000000000000000, 0.7071067811865482389 ) ) ;
#22530=ORIENTED_EDGE ( 'NONE', *, *, #17053, .T. ) ;
#22680=CARTESIAN_POINT ( 'NONE',  ( 0.000000000000000000, 0.000000000000000000, 53.00000000000000000 ) ) ;
#22805=CIRCLE ( 'NONE', #18126, 9.000000000000000000 ) ;
#22811=FACE_OUTER_BOUND ( 'NONE', #10773, .T. ) ;
#22822=ADVANCED_FACE ( 'NONE', ( #17852 ), #16129, .F. ) ;
#22949=DIRECTION ( 'NONE',  ( -0.000000000000000000, -0.000000000000000000, -1.000000000000000000 ) ) ;
#22967=ORIENTED_EDGE ( 'NONE', *, *, #2456, .T. ) ;
#23131=CARTESIAN_POINT ( 'NONE',  ( 0.000000000000000000, 0.000000000000000000, 53.00000000000000000 ) ) ;
#23267=FACE_OUTER_BOUND ( 'NONE', #20040, .T. ) ;
#23406=DIRECTION ( 'NONE',  ( -0.000000000000000000, -0.000000000000000000, 1.000000000000000000 ) ) ;
#23434=CARTESIAN_POINT ( 'NONE',  ( -9.000000000000000000, 0.000000000000000000, 0.9999999999999940048 ) ) ;
#23622=DIRECTION ( 'NONE',  ( 1.000000000000000000, 0.000000000000000000, 0.000000000000000000 ) ) ;
#23741=SHAPE_REPRESENTATION ( 'Part11^Assembly Idle gear', ( #8005 ), #2575 ) ;
#23772=VERTEX_POINT ( 'NONE', #6006 ) ;
#23823=AXIS2_PLACEMENT_3D ( 'NONE', #5295, #5167, #1627 ) ;
#23854=VECTOR ( 'NONE', #5217, 999.9999999999998863 ) ;
#23986=ORIENTED_EDGE ( 'NONE', *, *, #14745, .T. ) ;
#24016=AXIS2_PLACEMENT_3D ( 'NONE', #23131, #6540, #17499 ) ;
#24065=FACE_OUTER_BOUND ( 'NONE', #10874, .T. ) ;
#24135=COLOUR_RGB('Light Blue',0.38,0.62,0.78);
#24136=FILL_AREA_STYLE_COLOUR('',#24135);
#24137=FILL_AREA_STYLE('',(#24136));
#24138=SURFACE_STYLE_FILL_AREA(#24137);
#24139=SURFACE_SIDE_STYLE('',(#24138));
#24140=SURFACE_STYLE_USAGE(.BOTH.,#24139);
#24141=PRESENTATION_STYLE_ASSIGNMENT((#24140));
ENDSEC;
END-ISO-10303-21;
